ISO-10303-21;
HEADER;
/* Generated by software containing ST-Developer
 * from STEP Tools, Inc. (www.steptools.com) 
 */

FILE_DESCRIPTION(
/* description */ ('STEP AP214'),
/* implementation_level */ '2;1');

FILE_NAME(
/* name */ 'P_Torque Wrench_Handle Grip Drive Nut_1012.step',
/* time_stamp */ '2026-10-07T12:49:37-07:00',
/* author */ (''),
/* organization */ (''),
/* preprocessor_version */ 'ST-DEVELOPER v20.2',
/* originating_system */ 'Autodesk Translation Framework v15.15.0.0',
/* authorisation */ '');

FILE_SCHEMA (('AUTOMOTIVE_DESIGN { 1 0 10303 214 3 1 1 }'));
ENDSEC;

DATA;
#10=MECHANICAL_DESIGN_GEOMETRIC_PRESENTATION_REPRESENTATION('',(#317),#33016);
#209=(
BOUNDED_CURVE()
B_SPLINE_CURVE(2,(#32837,#32838,#32839),.UNSPECIFIED.,.F.,.F.)
B_SPLINE_CURVE_WITH_KNOTS((3,3),(-2.09220112582086,-1.49953837172718),
 .UNSPECIFIED.)
CURVE()
GEOMETRIC_REPRESENTATION_ITEM()
RATIONAL_B_SPLINE_CURVE((1.46412629524771,1.56864298547016,1.5767033028551))
REPRESENTATION_ITEM('')
);
#210=(
BOUNDED_CURVE()
B_SPLINE_CURVE(2,(#32841,#32842,#32843),.UNSPECIFIED.,.F.,.F.)
B_SPLINE_CURVE_WITH_KNOTS((3,3),(-1.40048737572359,-0.807824621629909),
 .UNSPECIFIED.)
CURVE()
GEOMETRIC_REPRESENTATION_ITEM()
RATIONAL_B_SPLINE_CURVE((1.5767033028551,1.56864298547016,1.46412629524771))
REPRESENTATION_ITEM('')
);
#211=(
BOUNDED_CURVE()
B_SPLINE_CURVE(2,(#32846,#32847,#32848),.UNSPECIFIED.,.F.,.F.)
B_SPLINE_CURVE_WITH_KNOTS((3,3),(-2.09213650825597,-1.4994860626003),
 .UNSPECIFIED.)
CURVE()
GEOMETRIC_REPRESENTATION_ITEM()
RATIONAL_B_SPLINE_CURVE((1.46410161513778,1.56861654357001,1.57667672508584))
REPRESENTATION_ITEM('')
);
#212=(
BOUNDED_CURVE()
B_SPLINE_CURVE(2,(#32849,#32850,#32851),.UNSPECIFIED.,.F.,.F.)
B_SPLINE_CURVE_WITH_KNOTS((3,3),(-1.4004371236908,-0.807786678035135),
 .UNSPECIFIED.)
CURVE()
GEOMETRIC_REPRESENTATION_ITEM()
RATIONAL_B_SPLINE_CURVE((1.57667672508584,1.56861654357001,1.46410161513778))
REPRESENTATION_ITEM('')
);
#213=(
BOUNDED_CURVE()
B_SPLINE_CURVE(2,(#32853,#32854,#32855),.UNSPECIFIED.,.F.,.F.)
B_SPLINE_CURVE_WITH_KNOTS((3,3),(-2.09220112574637,-1.49953837166687),
 .UNSPECIFIED.)
CURVE()
GEOMETRIC_REPRESENTATION_ITEM()
RATIONAL_B_SPLINE_CURVE((1.46412629521926,1.56864298543969,1.57670330282446))
REPRESENTATION_ITEM('')
);
#214=(
BOUNDED_CURVE()
B_SPLINE_CURVE(2,(#32857,#32858,#32859),.UNSPECIFIED.,.F.,.F.)
B_SPLINE_CURVE_WITH_KNOTS((3,3),(-1.40048737566568,-0.80782462158617),
 .UNSPECIFIED.)
CURVE()
GEOMETRIC_REPRESENTATION_ITEM()
RATIONAL_B_SPLINE_CURVE((1.57670330282446,1.56864298543969,1.46412629521926))
REPRESENTATION_ITEM('')
);
#215=(
BOUNDED_CURVE()
B_SPLINE_CURVE(2,(#32862,#32863,#32864),.UNSPECIFIED.,.F.,.F.)
B_SPLINE_CURVE_WITH_KNOTS((3,3),(-2.09213650825596,-1.49948606260029),
 .UNSPECIFIED.)
CURVE()
GEOMETRIC_REPRESENTATION_ITEM()
RATIONAL_B_SPLINE_CURVE((1.46410161513778,1.56861654357001,1.57667672508584))
REPRESENTATION_ITEM('')
);
#216=(
BOUNDED_CURVE()
B_SPLINE_CURVE(2,(#32865,#32866,#32867),.UNSPECIFIED.,.F.,.F.)
B_SPLINE_CURVE_WITH_KNOTS((3,3),(-1.40043712369081,-0.807786678035134),
 .UNSPECIFIED.)
CURVE()
GEOMETRIC_REPRESENTATION_ITEM()
RATIONAL_B_SPLINE_CURVE((1.57667672508584,1.56861654357001,1.46410161513778))
REPRESENTATION_ITEM('')
);
#217=(
BOUNDED_CURVE()
B_SPLINE_CURVE(2,(#32869,#32870,#32871),.UNSPECIFIED.,.F.,.F.)
B_SPLINE_CURVE_WITH_KNOTS((3,3),(-2.09220112574637,-1.49953837166686),
 .UNSPECIFIED.)
CURVE()
GEOMETRIC_REPRESENTATION_ITEM()
RATIONAL_B_SPLINE_CURVE((1.46412629521926,1.56864298543969,1.57670330282446))
REPRESENTATION_ITEM('')
);
#218=(
BOUNDED_CURVE()
B_SPLINE_CURVE(2,(#32873,#32874,#32875),.UNSPECIFIED.,.F.,.F.)
B_SPLINE_CURVE_WITH_KNOTS((3,3),(-1.40048737566568,-0.80782462158617),
 .UNSPECIFIED.)
CURVE()
GEOMETRIC_REPRESENTATION_ITEM()
RATIONAL_B_SPLINE_CURVE((1.57670330282446,1.56864298543969,1.46412629521926))
REPRESENTATION_ITEM('')
);
#219=(
BOUNDED_CURVE()
B_SPLINE_CURVE(2,(#32878,#32879,#32880),.UNSPECIFIED.,.F.,.F.)
B_SPLINE_CURVE_WITH_KNOTS((3,3),(-2.09213650825596,-1.49948606260028),
 .UNSPECIFIED.)
CURVE()
GEOMETRIC_REPRESENTATION_ITEM()
RATIONAL_B_SPLINE_CURVE((1.46410161513778,1.56861654357001,1.57667672508584))
REPRESENTATION_ITEM('')
);
#220=(
BOUNDED_CURVE()
B_SPLINE_CURVE(2,(#32881,#32882,#32883),.UNSPECIFIED.,.F.,.F.)
B_SPLINE_CURVE_WITH_KNOTS((3,3),(-1.40043712369082,-0.807786678035136),
 .UNSPECIFIED.)
CURVE()
GEOMETRIC_REPRESENTATION_ITEM()
RATIONAL_B_SPLINE_CURVE((1.57667672508584,1.56861654357001,1.46410161513778))
REPRESENTATION_ITEM('')
);
#221=(
BOUNDED_CURVE()
B_SPLINE_CURVE(2,(#32885,#32886,#32887),.UNSPECIFIED.,.F.,.F.)
B_SPLINE_CURVE_WITH_KNOTS((3,3),(-2.09220112582086,-1.49953837172717),
 .UNSPECIFIED.)
CURVE()
GEOMETRIC_REPRESENTATION_ITEM()
RATIONAL_B_SPLINE_CURVE((1.46412629524771,1.56864298547016,1.5767033028551))
REPRESENTATION_ITEM('')
);
#222=(
BOUNDED_CURVE()
B_SPLINE_CURVE(2,(#32889,#32890,#32891),.UNSPECIFIED.,.F.,.F.)
B_SPLINE_CURVE_WITH_KNOTS((3,3),(-1.4004873757236,-0.80782462162991),
 .UNSPECIFIED.)
CURVE()
GEOMETRIC_REPRESENTATION_ITEM()
RATIONAL_B_SPLINE_CURVE((1.5767033028551,1.56864298547016,1.46412629524771))
REPRESENTATION_ITEM('')
);
#223=(
BOUNDED_CURVE()
B_SPLINE_CURVE(2,(#32894,#32895,#32896),.UNSPECIFIED.,.F.,.F.)
B_SPLINE_CURVE_WITH_KNOTS((3,3),(-2.09213650825596,-1.4994860626003),
 .UNSPECIFIED.)
CURVE()
GEOMETRIC_REPRESENTATION_ITEM()
RATIONAL_B_SPLINE_CURVE((1.46410161513778,1.56861654357001,1.57667672508584))
REPRESENTATION_ITEM('')
);
#224=(
BOUNDED_CURVE()
B_SPLINE_CURVE(2,(#32897,#32898,#32899),.UNSPECIFIED.,.F.,.F.)
B_SPLINE_CURVE_WITH_KNOTS((3,3),(-1.40043712369081,-0.807786678035135),
 .UNSPECIFIED.)
CURVE()
GEOMETRIC_REPRESENTATION_ITEM()
RATIONAL_B_SPLINE_CURVE((1.57667672508584,1.56861654357001,1.46410161513778))
REPRESENTATION_ITEM('')
);
#225=(
BOUNDED_CURVE()
B_SPLINE_CURVE(2,(#32901,#32902,#32903),.UNSPECIFIED.,.F.,.F.)
B_SPLINE_CURVE_WITH_KNOTS((3,3),(-2.09220112574637,-1.49953837166688),
 .UNSPECIFIED.)
CURVE()
GEOMETRIC_REPRESENTATION_ITEM()
RATIONAL_B_SPLINE_CURVE((1.46412629521926,1.56864298543968,1.57670330282446))
REPRESENTATION_ITEM('')
);
#226=(
BOUNDED_CURVE()
B_SPLINE_CURVE(2,(#32905,#32906,#32907),.UNSPECIFIED.,.F.,.F.)
B_SPLINE_CURVE_WITH_KNOTS((3,3),(-1.40048737566567,-0.80782462158617),
 .UNSPECIFIED.)
CURVE()
GEOMETRIC_REPRESENTATION_ITEM()
RATIONAL_B_SPLINE_CURVE((1.57670330282446,1.56864298543968,1.46412629521926))
REPRESENTATION_ITEM('')
);
#227=(
BOUNDED_CURVE()
B_SPLINE_CURVE(2,(#32910,#32911,#32912),.UNSPECIFIED.,.F.,.F.)
B_SPLINE_CURVE_WITH_KNOTS((3,3),(-2.09213650825596,-1.4994860626003),
 .UNSPECIFIED.)
CURVE()
GEOMETRIC_REPRESENTATION_ITEM()
RATIONAL_B_SPLINE_CURVE((1.46410161513778,1.56861654357001,1.57667672508584))
REPRESENTATION_ITEM('')
);
#228=(
BOUNDED_CURVE()
B_SPLINE_CURVE(2,(#32913,#32914,#32915),.UNSPECIFIED.,.F.,.F.)
B_SPLINE_CURVE_WITH_KNOTS((3,3),(-1.4004371236908,-0.807786678035133),
 .UNSPECIFIED.)
CURVE()
GEOMETRIC_REPRESENTATION_ITEM()
RATIONAL_B_SPLINE_CURVE((1.57667672508584,1.56861654357001,1.46410161513778))
REPRESENTATION_ITEM('')
);
#229=(
BOUNDED_CURVE()
B_SPLINE_CURVE(2,(#32917,#32918,#32919),.UNSPECIFIED.,.F.,.F.)
B_SPLINE_CURVE_WITH_KNOTS((3,3),(-2.09220112574637,-1.49953837166687),
 .UNSPECIFIED.)
CURVE()
GEOMETRIC_REPRESENTATION_ITEM()
RATIONAL_B_SPLINE_CURVE((1.46412629521926,1.56864298543969,1.57670330282446))
REPRESENTATION_ITEM('')
);
#230=(
BOUNDED_CURVE()
B_SPLINE_CURVE(2,(#32920,#32921,#32922),.UNSPECIFIED.,.F.,.F.)
B_SPLINE_CURVE_WITH_KNOTS((3,3),(-1.40048737566567,-0.807824621586168),
 .UNSPECIFIED.)
CURVE()
GEOMETRIC_REPRESENTATION_ITEM()
RATIONAL_B_SPLINE_CURVE((1.57670330282446,1.56864298543968,1.46412629521926))
REPRESENTATION_ITEM('')
);
#231=(
BOUNDED_CURVE()
B_SPLINE_CURVE(2,(#32923,#32924,#32925),.UNSPECIFIED.,.F.,.F.)
B_SPLINE_CURVE_WITH_KNOTS((3,3),(-2.09213650825597,-1.49948606260029),
 .UNSPECIFIED.)
CURVE()
GEOMETRIC_REPRESENTATION_ITEM()
RATIONAL_B_SPLINE_CURVE((1.46410161513778,1.56861654357001,1.57667672508584))
REPRESENTATION_ITEM('')
);
#232=(
BOUNDED_CURVE()
B_SPLINE_CURVE(2,(#32926,#32927,#32928),.UNSPECIFIED.,.F.,.F.)
B_SPLINE_CURVE_WITH_KNOTS((3,3),(-1.40043712369081,-0.807786678035134),
 .UNSPECIFIED.)
CURVE()
GEOMETRIC_REPRESENTATION_ITEM()
RATIONAL_B_SPLINE_CURVE((1.57667672508584,1.56861654357001,1.46410161513778))
REPRESENTATION_ITEM('')
);
#259=SHAPE_REPRESENTATION_RELATIONSHIP('SRR','None',#33154,#286);
#286=ADVANCED_BREP_SHAPE_REPRESENTATION('',(#344),#33015);
#317=STYLED_ITEM('',(#33289),#344);
#344=MANIFOLD_SOLID_BREP('Body1',#9968);
#372=CONICAL_SURFACE('',#11210,6.50555349946514,0.785398163397448);
#373=CONICAL_SURFACE('',#11211,6.50555349946514,0.785398163397448);
#374=CONICAL_SURFACE('',#11212,6.50555349946514,0.785398163397448);
#375=CONICAL_SURFACE('',#11213,6.50555349946514,0.785398163397448);
#376=CONICAL_SURFACE('',#11214,6.50555349946514,0.785398163397448);
#377=CONICAL_SURFACE('',#11215,6.50555349946514,0.785398163397448);
#378=CONICAL_SURFACE('',#11216,6.50555349946514,0.785398163397448);
#379=CONICAL_SURFACE('',#11217,6.50555349946514,0.785398163397448);
#380=CONICAL_SURFACE('',#11218,6.50555349946514,0.785398163397448);
#381=CONICAL_SURFACE('',#11219,6.50555349946514,0.785398163397448);
#382=CONICAL_SURFACE('',#11220,6.50555349946514,0.785398163397448);
#383=CONICAL_SURFACE('',#11221,6.50555349946514,0.785398163397448);
#552=FACE_BOUND('',#2190,.T.);
#553=FACE_BOUND('',#2192,.T.);
#1012=PLANE('',#11188);
#1013=PLANE('',#11196);
#1014=PLANE('',#11204);
#1015=PLANE('',#11205);
#1016=PLANE('',#11206);
#1017=PLANE('',#11207);
#1018=PLANE('',#11208);
#1019=PLANE('',#11209);
#1555=FACE_OUTER_BOUND('',#2189,.T.);
#1556=FACE_OUTER_BOUND('',#2191,.T.);
#1557=FACE_OUTER_BOUND('',#2193,.T.);
#1558=FACE_OUTER_BOUND('',#2194,.T.);
#1559=FACE_OUTER_BOUND('',#2195,.T.);
#1560=FACE_OUTER_BOUND('',#2196,.T.);
#1561=FACE_OUTER_BOUND('',#2197,.T.);
#1562=FACE_OUTER_BOUND('',#2198,.T.);
#1563=FACE_OUTER_BOUND('',#2199,.T.);
#1564=FACE_OUTER_BOUND('',#2200,.T.);
#1565=FACE_OUTER_BOUND('',#2201,.T.);
#1566=FACE_OUTER_BOUND('',#2202,.T.);
#1567=FACE_OUTER_BOUND('',#2203,.T.);
#1568=FACE_OUTER_BOUND('',#2204,.T.);
#1569=FACE_OUTER_BOUND('',#2205,.T.);
#1570=FACE_OUTER_BOUND('',#2206,.T.);
#1571=FACE_OUTER_BOUND('',#2207,.T.);
#1572=FACE_OUTER_BOUND('',#2208,.T.);
#1573=FACE_OUTER_BOUND('',#2209,.T.);
#1574=FACE_OUTER_BOUND('',#2210,.T.);
#1575=FACE_OUTER_BOUND('',#2211,.T.);
#2189=EDGE_LOOP('',(#9108,#9109,#9110,#9111,#9112,#9113,#9114,#9115,#9116,
#9117,#9118,#9119));
#2190=EDGE_LOOP('',(#9120));
#2191=EDGE_LOOP('',(#9121,#9122,#9123,#9124,#9125,#9126,#9127,#9128,#9129,
#9130,#9131,#9132));
#2192=EDGE_LOOP('',(#9133));
#2193=EDGE_LOOP('',(#9134,#9135,#9136,#9137,#9138,#9139,#9140,#9141));
#2194=EDGE_LOOP('',(#9142,#9143,#9144,#9145,#9146,#9147,#9148,#9149));
#2195=EDGE_LOOP('',(#9150,#9151,#9152,#9153,#9154,#9155,#9156,#9157));
#2196=EDGE_LOOP('',(#9158,#9159,#9160,#9161,#9162,#9163,#9164,#9165));
#2197=EDGE_LOOP('',(#9166,#9167,#9168,#9169,#9170,#9171,#9172,#9173));
#2198=EDGE_LOOP('',(#9174,#9175,#9176,#9177,#9178,#9179,#9180,#9181));
#2199=EDGE_LOOP('',(#9182,#9183,#9184));
#2200=EDGE_LOOP('',(#9185,#9186,#9187));
#2201=EDGE_LOOP('',(#9188,#9189,#9190));
#2202=EDGE_LOOP('',(#9191,#9192,#9193));
#2203=EDGE_LOOP('',(#9194,#9195,#9196));
#2204=EDGE_LOOP('',(#9197,#9198,#9199));
#2205=EDGE_LOOP('',(#9200,#9201,#9202));
#2206=EDGE_LOOP('',(#9203,#9204,#9205));
#2207=EDGE_LOOP('',(#9206,#9207,#9208));
#2208=EDGE_LOOP('',(#9209,#9210,#9211));
#2209=EDGE_LOOP('',(#9212,#9213,#9214));
#2210=EDGE_LOOP('',(#9215,#9216,#9217));
#2211=EDGE_LOOP('',(#9218,#9219,#9220,#9221));
#2586=CIRCLE('',#11189,6.50555349946514);
#2587=CIRCLE('',#11190,6.50555349946514);
#2588=CIRCLE('',#11191,6.50555349946514);
#2589=CIRCLE('',#11192,6.50555349946514);
#2590=CIRCLE('',#11193,6.50555349946514);
#2591=CIRCLE('',#11194,6.50555349946514);
#2592=CIRCLE('',#11195,3.5);
#2593=CIRCLE('',#11197,6.50555349946514);
#2594=CIRCLE('',#11198,6.50555349946514);
#2595=CIRCLE('',#11199,6.50555349946514);
#2596=CIRCLE('',#11200,6.50555349946514);
#2597=CIRCLE('',#11201,6.50555349946514);
#2598=CIRCLE('',#11202,6.50555349946514);
#2599=CIRCLE('',#11203,3.5);
#3331=LINE('',#32782,#4081);
#3332=LINE('',#32786,#4082);
#3333=LINE('',#32790,#4083);
#3334=LINE('',#32794,#4084);
#3335=LINE('',#32798,#4085);
#3336=LINE('',#32802,#4086);
#3337=LINE('',#32811,#4087);
#3338=LINE('',#32815,#4088);
#3339=LINE('',#32819,#4089);
#3340=LINE('',#32823,#4090);
#3341=LINE('',#32827,#4091);
#3342=LINE('',#32830,#4092);
#3343=LINE('',#32836,#4093);
#3344=LINE('',#32845,#4094);
#3345=LINE('',#32861,#4095);
#3346=LINE('',#32877,#4096);
#3347=LINE('',#32893,#4097);
#3348=LINE('',#32909,#4098);
#3349=LINE('',#32942,#4099);
#4081=VECTOR('',#13808,1000.);
#4082=VECTOR('',#13811,1000.);
#4083=VECTOR('',#13814,1000.);
#4084=VECTOR('',#13817,1000.);
#4085=VECTOR('',#13820,1000.);
#4086=VECTOR('',#13823,1000.);
#4087=VECTOR('',#13832,1000.);
#4088=VECTOR('',#13835,1000.);
#4089=VECTOR('',#13838,1000.);
#4090=VECTOR('',#13841,1000.);
#4091=VECTOR('',#13844,1000.);
#4092=VECTOR('',#13847,1000.);
#4093=VECTOR('',#13852,1000.);
#4094=VECTOR('',#13853,1000.);
#4095=VECTOR('',#13856,1000.);
#4096=VECTOR('',#13859,1000.);
#4097=VECTOR('',#13862,1000.);
#4098=VECTOR('',#13865,1000.);
#4099=VECTOR('',#13894,3.5);
#4987=VERTEX_POINT('',#32780);
#4988=VERTEX_POINT('',#32781);
#4989=VERTEX_POINT('',#32783);
#4990=VERTEX_POINT('',#32785);
#4991=VERTEX_POINT('',#32787);
#4992=VERTEX_POINT('',#32789);
#4993=VERTEX_POINT('',#32791);
#4994=VERTEX_POINT('',#32793);
#4995=VERTEX_POINT('',#32795);
#4996=VERTEX_POINT('',#32797);
#4997=VERTEX_POINT('',#32799);
#4998=VERTEX_POINT('',#32801);
#4999=VERTEX_POINT('',#32804);
#5000=VERTEX_POINT('',#32807);
#5001=VERTEX_POINT('',#32808);
#5002=VERTEX_POINT('',#32810);
#5003=VERTEX_POINT('',#32812);
#5004=VERTEX_POINT('',#32814);
#5005=VERTEX_POINT('',#32816);
#5006=VERTEX_POINT('',#32818);
#5007=VERTEX_POINT('',#32820);
#5008=VERTEX_POINT('',#32822);
#5009=VERTEX_POINT('',#32824);
#5010=VERTEX_POINT('',#32826);
#5011=VERTEX_POINT('',#32828);
#5012=VERTEX_POINT('',#32831);
#5013=VERTEX_POINT('',#32834);
#5014=VERTEX_POINT('',#32835);
#5015=VERTEX_POINT('',#32840);
#5016=VERTEX_POINT('',#32844);
#5017=VERTEX_POINT('',#32856);
#5018=VERTEX_POINT('',#32860);
#5019=VERTEX_POINT('',#32872);
#5020=VERTEX_POINT('',#32876);
#5021=VERTEX_POINT('',#32888);
#5022=VERTEX_POINT('',#32892);
#5023=VERTEX_POINT('',#32904);
#5024=VERTEX_POINT('',#32908);
#6367=EDGE_CURVE('',#4987,#4988,#3331,.T.);
#6368=EDGE_CURVE('',#4987,#4989,#2586,.T.);
#6369=EDGE_CURVE('',#4990,#4989,#3332,.T.);
#6370=EDGE_CURVE('',#4990,#4991,#2587,.T.);
#6371=EDGE_CURVE('',#4992,#4991,#3333,.T.);
#6372=EDGE_CURVE('',#4992,#4993,#2588,.T.);
#6373=EDGE_CURVE('',#4994,#4993,#3334,.T.);
#6374=EDGE_CURVE('',#4994,#4995,#2589,.T.);
#6375=EDGE_CURVE('',#4996,#4995,#3335,.T.);
#6376=EDGE_CURVE('',#4996,#4997,#2590,.T.);
#6377=EDGE_CURVE('',#4998,#4997,#3336,.T.);
#6378=EDGE_CURVE('',#4998,#4988,#2591,.T.);
#6379=EDGE_CURVE('',#4999,#4999,#2592,.T.);
#6380=EDGE_CURVE('',#5000,#5001,#2593,.T.);
#6381=EDGE_CURVE('',#5000,#5002,#3337,.T.);
#6382=EDGE_CURVE('',#5003,#5002,#2594,.T.);
#6383=EDGE_CURVE('',#5003,#5004,#3338,.T.);
#6384=EDGE_CURVE('',#5005,#5004,#2595,.T.);
#6385=EDGE_CURVE('',#5005,#5006,#3339,.T.);
#6386=EDGE_CURVE('',#5007,#5006,#2596,.T.);
#6387=EDGE_CURVE('',#5007,#5008,#3340,.T.);
#6388=EDGE_CURVE('',#5009,#5008,#2597,.T.);
#6389=EDGE_CURVE('',#5009,#5010,#3341,.T.);
#6390=EDGE_CURVE('',#5011,#5010,#2598,.T.);
#6391=EDGE_CURVE('',#5011,#5001,#3342,.T.);
#6392=EDGE_CURVE('',#5012,#5012,#2599,.T.);
#6393=EDGE_CURVE('',#5013,#5014,#3343,.T.);
#6394=EDGE_CURVE('',#5014,#4996,#209,.T.);
#6395=EDGE_CURVE('',#4995,#5015,#210,.T.);
#6396=EDGE_CURVE('',#5016,#5015,#3344,.T.);
#6397=EDGE_CURVE('',#5016,#5006,#211,.T.);
#6398=EDGE_CURVE('',#5005,#5013,#212,.T.);
#6399=EDGE_CURVE('',#5015,#4994,#213,.T.);
#6400=EDGE_CURVE('',#4993,#5017,#214,.T.);
#6401=EDGE_CURVE('',#5018,#5017,#3345,.T.);
#6402=EDGE_CURVE('',#5018,#5008,#215,.T.);
#6403=EDGE_CURVE('',#5007,#5016,#216,.T.);
#6404=EDGE_CURVE('',#5017,#4992,#217,.T.);
#6405=EDGE_CURVE('',#4991,#5019,#218,.T.);
#6406=EDGE_CURVE('',#5020,#5019,#3346,.T.);
#6407=EDGE_CURVE('',#5020,#5010,#219,.T.);
#6408=EDGE_CURVE('',#5009,#5018,#220,.T.);
#6409=EDGE_CURVE('',#5019,#4990,#221,.T.);
#6410=EDGE_CURVE('',#4989,#5021,#222,.T.);
#6411=EDGE_CURVE('',#5022,#5021,#3347,.T.);
#6412=EDGE_CURVE('',#5022,#5001,#223,.T.);
#6413=EDGE_CURVE('',#5011,#5020,#224,.T.);
#6414=EDGE_CURVE('',#5021,#4987,#225,.T.);
#6415=EDGE_CURVE('',#4988,#5023,#226,.T.);
#6416=EDGE_CURVE('',#5024,#5023,#3348,.T.);
#6417=EDGE_CURVE('',#5024,#5002,#227,.T.);
#6418=EDGE_CURVE('',#5000,#5022,#228,.T.);
#6419=EDGE_CURVE('',#5023,#4998,#229,.T.);
#6420=EDGE_CURVE('',#4997,#5014,#230,.T.);
#6421=EDGE_CURVE('',#5013,#5004,#231,.T.);
#6422=EDGE_CURVE('',#5003,#5024,#232,.T.);
#6423=EDGE_CURVE('',#5012,#4999,#3349,.T.);
#9108=ORIENTED_EDGE('',*,*,#6367,.F.);
#9109=ORIENTED_EDGE('',*,*,#6368,.T.);
#9110=ORIENTED_EDGE('',*,*,#6369,.F.);
#9111=ORIENTED_EDGE('',*,*,#6370,.T.);
#9112=ORIENTED_EDGE('',*,*,#6371,.F.);
#9113=ORIENTED_EDGE('',*,*,#6372,.T.);
#9114=ORIENTED_EDGE('',*,*,#6373,.F.);
#9115=ORIENTED_EDGE('',*,*,#6374,.T.);
#9116=ORIENTED_EDGE('',*,*,#6375,.F.);
#9117=ORIENTED_EDGE('',*,*,#6376,.T.);
#9118=ORIENTED_EDGE('',*,*,#6377,.F.);
#9119=ORIENTED_EDGE('',*,*,#6378,.T.);
#9120=ORIENTED_EDGE('',*,*,#6379,.F.);
#9121=ORIENTED_EDGE('',*,*,#6380,.F.);
#9122=ORIENTED_EDGE('',*,*,#6381,.T.);
#9123=ORIENTED_EDGE('',*,*,#6382,.F.);
#9124=ORIENTED_EDGE('',*,*,#6383,.T.);
#9125=ORIENTED_EDGE('',*,*,#6384,.F.);
#9126=ORIENTED_EDGE('',*,*,#6385,.T.);
#9127=ORIENTED_EDGE('',*,*,#6386,.F.);
#9128=ORIENTED_EDGE('',*,*,#6387,.T.);
#9129=ORIENTED_EDGE('',*,*,#6388,.F.);
#9130=ORIENTED_EDGE('',*,*,#6389,.T.);
#9131=ORIENTED_EDGE('',*,*,#6390,.F.);
#9132=ORIENTED_EDGE('',*,*,#6391,.T.);
#9133=ORIENTED_EDGE('',*,*,#6392,.F.);
#9134=ORIENTED_EDGE('',*,*,#6393,.T.);
#9135=ORIENTED_EDGE('',*,*,#6394,.T.);
#9136=ORIENTED_EDGE('',*,*,#6375,.T.);
#9137=ORIENTED_EDGE('',*,*,#6395,.T.);
#9138=ORIENTED_EDGE('',*,*,#6396,.F.);
#9139=ORIENTED_EDGE('',*,*,#6397,.T.);
#9140=ORIENTED_EDGE('',*,*,#6385,.F.);
#9141=ORIENTED_EDGE('',*,*,#6398,.T.);
#9142=ORIENTED_EDGE('',*,*,#6396,.T.);
#9143=ORIENTED_EDGE('',*,*,#6399,.T.);
#9144=ORIENTED_EDGE('',*,*,#6373,.T.);
#9145=ORIENTED_EDGE('',*,*,#6400,.T.);
#9146=ORIENTED_EDGE('',*,*,#6401,.F.);
#9147=ORIENTED_EDGE('',*,*,#6402,.T.);
#9148=ORIENTED_EDGE('',*,*,#6387,.F.);
#9149=ORIENTED_EDGE('',*,*,#6403,.T.);
#9150=ORIENTED_EDGE('',*,*,#6401,.T.);
#9151=ORIENTED_EDGE('',*,*,#6404,.T.);
#9152=ORIENTED_EDGE('',*,*,#6371,.T.);
#9153=ORIENTED_EDGE('',*,*,#6405,.T.);
#9154=ORIENTED_EDGE('',*,*,#6406,.F.);
#9155=ORIENTED_EDGE('',*,*,#6407,.T.);
#9156=ORIENTED_EDGE('',*,*,#6389,.F.);
#9157=ORIENTED_EDGE('',*,*,#6408,.T.);
#9158=ORIENTED_EDGE('',*,*,#6406,.T.);
#9159=ORIENTED_EDGE('',*,*,#6409,.T.);
#9160=ORIENTED_EDGE('',*,*,#6369,.T.);
#9161=ORIENTED_EDGE('',*,*,#6410,.T.);
#9162=ORIENTED_EDGE('',*,*,#6411,.F.);
#9163=ORIENTED_EDGE('',*,*,#6412,.T.);
#9164=ORIENTED_EDGE('',*,*,#6391,.F.);
#9165=ORIENTED_EDGE('',*,*,#6413,.T.);
#9166=ORIENTED_EDGE('',*,*,#6411,.T.);
#9167=ORIENTED_EDGE('',*,*,#6414,.T.);
#9168=ORIENTED_EDGE('',*,*,#6367,.T.);
#9169=ORIENTED_EDGE('',*,*,#6415,.T.);
#9170=ORIENTED_EDGE('',*,*,#6416,.F.);
#9171=ORIENTED_EDGE('',*,*,#6417,.T.);
#9172=ORIENTED_EDGE('',*,*,#6381,.F.);
#9173=ORIENTED_EDGE('',*,*,#6418,.T.);
#9174=ORIENTED_EDGE('',*,*,#6416,.T.);
#9175=ORIENTED_EDGE('',*,*,#6419,.T.);
#9176=ORIENTED_EDGE('',*,*,#6377,.T.);
#9177=ORIENTED_EDGE('',*,*,#6420,.T.);
#9178=ORIENTED_EDGE('',*,*,#6393,.F.);
#9179=ORIENTED_EDGE('',*,*,#6421,.T.);
#9180=ORIENTED_EDGE('',*,*,#6383,.F.);
#9181=ORIENTED_EDGE('',*,*,#6422,.T.);
#9182=ORIENTED_EDGE('',*,*,#6422,.F.);
#9183=ORIENTED_EDGE('',*,*,#6382,.T.);
#9184=ORIENTED_EDGE('',*,*,#6417,.F.);
#9185=ORIENTED_EDGE('',*,*,#6384,.T.);
#9186=ORIENTED_EDGE('',*,*,#6421,.F.);
#9187=ORIENTED_EDGE('',*,*,#6398,.F.);
#9188=ORIENTED_EDGE('',*,*,#6403,.F.);
#9189=ORIENTED_EDGE('',*,*,#6386,.T.);
#9190=ORIENTED_EDGE('',*,*,#6397,.F.);
#9191=ORIENTED_EDGE('',*,*,#6408,.F.);
#9192=ORIENTED_EDGE('',*,*,#6388,.T.);
#9193=ORIENTED_EDGE('',*,*,#6402,.F.);
#9194=ORIENTED_EDGE('',*,*,#6413,.F.);
#9195=ORIENTED_EDGE('',*,*,#6390,.T.);
#9196=ORIENTED_EDGE('',*,*,#6407,.F.);
#9197=ORIENTED_EDGE('',*,*,#6418,.F.);
#9198=ORIENTED_EDGE('',*,*,#6380,.T.);
#9199=ORIENTED_EDGE('',*,*,#6412,.F.);
#9200=ORIENTED_EDGE('',*,*,#6378,.F.);
#9201=ORIENTED_EDGE('',*,*,#6419,.F.);
#9202=ORIENTED_EDGE('',*,*,#6415,.F.);
#9203=ORIENTED_EDGE('',*,*,#6420,.F.);
#9204=ORIENTED_EDGE('',*,*,#6376,.F.);
#9205=ORIENTED_EDGE('',*,*,#6394,.F.);
#9206=ORIENTED_EDGE('',*,*,#6374,.F.);
#9207=ORIENTED_EDGE('',*,*,#6399,.F.);
#9208=ORIENTED_EDGE('',*,*,#6395,.F.);
#9209=ORIENTED_EDGE('',*,*,#6372,.F.);
#9210=ORIENTED_EDGE('',*,*,#6404,.F.);
#9211=ORIENTED_EDGE('',*,*,#6400,.F.);
#9212=ORIENTED_EDGE('',*,*,#6370,.F.);
#9213=ORIENTED_EDGE('',*,*,#6409,.F.);
#9214=ORIENTED_EDGE('',*,*,#6405,.F.);
#9215=ORIENTED_EDGE('',*,*,#6368,.F.);
#9216=ORIENTED_EDGE('',*,*,#6414,.F.);
#9217=ORIENTED_EDGE('',*,*,#6410,.F.);
#9218=ORIENTED_EDGE('',*,*,#6392,.T.);
#9219=ORIENTED_EDGE('',*,*,#6423,.T.);
#9220=ORIENTED_EDGE('',*,*,#6379,.T.);
#9221=ORIENTED_EDGE('',*,*,#6423,.F.);
#9385=CYLINDRICAL_SURFACE('',#11222,3.5);
#9921=ADVANCED_FACE('',(#1555,#552),#1012,.F.);
#9922=ADVANCED_FACE('',(#1556,#553),#1013,.T.);
#9923=ADVANCED_FACE('',(#1557),#1014,.F.);
#9924=ADVANCED_FACE('',(#1558),#1015,.F.);
#9925=ADVANCED_FACE('',(#1559),#1016,.F.);
#9926=ADVANCED_FACE('',(#1560),#1017,.F.);
#9927=ADVANCED_FACE('',(#1561),#1018,.F.);
#9928=ADVANCED_FACE('',(#1562),#1019,.F.);
#9929=ADVANCED_FACE('',(#1563),#372,.T.);
#9930=ADVANCED_FACE('',(#1564),#373,.T.);
#9931=ADVANCED_FACE('',(#1565),#374,.T.);
#9932=ADVANCED_FACE('',(#1566),#375,.T.);
#9933=ADVANCED_FACE('',(#1567),#376,.T.);
#9934=ADVANCED_FACE('',(#1568),#377,.T.);
#9935=ADVANCED_FACE('',(#1569),#378,.T.);
#9936=ADVANCED_FACE('',(#1570),#379,.T.);
#9937=ADVANCED_FACE('',(#1571),#380,.T.);
#9938=ADVANCED_FACE('',(#1572),#381,.T.);
#9939=ADVANCED_FACE('',(#1573),#382,.T.);
#9940=ADVANCED_FACE('',(#1574),#383,.T.);
#9941=ADVANCED_FACE('',(#1575),#9385,.F.);
#9968=CLOSED_SHELL('',(#9921,#9922,#9923,#9924,#9925,#9926,#9927,#9928,
#9929,#9930,#9931,#9932,#9933,#9934,#9935,#9936,#9937,#9938,#9939,#9940,
#9941));
#11187=AXIS2_PLACEMENT_3D('',#32778,#13804,#13805);
#11188=AXIS2_PLACEMENT_3D('',#32779,#13806,#13807);
#11189=AXIS2_PLACEMENT_3D('',#32784,#13809,#13810);
#11190=AXIS2_PLACEMENT_3D('',#32788,#13812,#13813);
#11191=AXIS2_PLACEMENT_3D('',#32792,#13815,#13816);
#11192=AXIS2_PLACEMENT_3D('',#32796,#13818,#13819);
#11193=AXIS2_PLACEMENT_3D('',#32800,#13821,#13822);
#11194=AXIS2_PLACEMENT_3D('',#32803,#13824,#13825);
#11195=AXIS2_PLACEMENT_3D('',#32805,#13826,#13827);
#11196=AXIS2_PLACEMENT_3D('',#32806,#13828,#13829);
#11197=AXIS2_PLACEMENT_3D('',#32809,#13830,#13831);
#11198=AXIS2_PLACEMENT_3D('',#32813,#13833,#13834);
#11199=AXIS2_PLACEMENT_3D('',#32817,#13836,#13837);
#11200=AXIS2_PLACEMENT_3D('',#32821,#13839,#13840);
#11201=AXIS2_PLACEMENT_3D('',#32825,#13842,#13843);
#11202=AXIS2_PLACEMENT_3D('',#32829,#13845,#13846);
#11203=AXIS2_PLACEMENT_3D('',#32832,#13848,#13849);
#11204=AXIS2_PLACEMENT_3D('',#32833,#13850,#13851);
#11205=AXIS2_PLACEMENT_3D('',#32852,#13854,#13855);
#11206=AXIS2_PLACEMENT_3D('',#32868,#13857,#13858);
#11207=AXIS2_PLACEMENT_3D('',#32884,#13860,#13861);
#11208=AXIS2_PLACEMENT_3D('',#32900,#13863,#13864);
#11209=AXIS2_PLACEMENT_3D('',#32916,#13866,#13867);
#11210=AXIS2_PLACEMENT_3D('',#32929,#13868,#13869);
#11211=AXIS2_PLACEMENT_3D('',#32930,#13870,#13871);
#11212=AXIS2_PLACEMENT_3D('',#32931,#13872,#13873);
#11213=AXIS2_PLACEMENT_3D('',#32932,#13874,#13875);
#11214=AXIS2_PLACEMENT_3D('',#32933,#13876,#13877);
#11215=AXIS2_PLACEMENT_3D('',#32934,#13878,#13879);
#11216=AXIS2_PLACEMENT_3D('',#32935,#13880,#13881);
#11217=AXIS2_PLACEMENT_3D('',#32936,#13882,#13883);
#11218=AXIS2_PLACEMENT_3D('',#32937,#13884,#13885);
#11219=AXIS2_PLACEMENT_3D('',#32938,#13886,#13887);
#11220=AXIS2_PLACEMENT_3D('',#32939,#13888,#13889);
#11221=AXIS2_PLACEMENT_3D('',#32940,#13890,#13891);
#11222=AXIS2_PLACEMENT_3D('',#32941,#13892,#13893);
#13804=DIRECTION('axis',(0.,0.,1.));
#13805=DIRECTION('refdir',(1.,0.,0.));
#13806=DIRECTION('center_axis',(0.,1.,0.));
#13807=DIRECTION('ref_axis',(0.,0.,1.));
#13808=DIRECTION('',(0.866025403784438,0.,0.5));
#13809=DIRECTION('center_axis',(0.,-1.,0.));
#13810=DIRECTION('ref_axis',(0.,0.,1.));
#13811=DIRECTION('',(1.1556266144132E-16,0.,1.));
#13812=DIRECTION('center_axis',(0.,-1.,0.));
#13813=DIRECTION('ref_axis',(0.,0.,1.));
#13814=DIRECTION('',(-0.866025403784439,0.,0.5));
#13815=DIRECTION('center_axis',(0.,-1.,0.));
#13816=DIRECTION('ref_axis',(0.,0.,1.));
#13817=DIRECTION('',(-0.866025403784438,0.,-0.5));
#13818=DIRECTION('center_axis',(0.,-1.,0.));
#13819=DIRECTION('ref_axis',(-8.88178419700125E-16,0.,1.));
#13820=DIRECTION('',(-1.1556266144132E-16,0.,-1.));
#13821=DIRECTION('center_axis',(0.,-1.,0.));
#13822=DIRECTION('ref_axis',(-8.88178419700125E-16,0.,1.));
#13823=DIRECTION('',(0.866025403784439,0.,-0.5));
#13824=DIRECTION('center_axis',(0.,-1.,0.));
#13825=DIRECTION('ref_axis',(0.,0.,1.));
#13826=DIRECTION('center_axis',(0.,-1.,0.));
#13827=DIRECTION('ref_axis',(0.,0.,-1.));
#13828=DIRECTION('center_axis',(0.,1.,0.));
#13829=DIRECTION('ref_axis',(0.,0.,1.));
#13830=DIRECTION('center_axis',(0.,-1.,0.));
#13831=DIRECTION('ref_axis',(0.,0.,1.));
#13832=DIRECTION('',(0.866025403784438,0.,0.5));
#13833=DIRECTION('center_axis',(0.,-1.,0.));
#13834=DIRECTION('ref_axis',(0.,0.,1.));
#13835=DIRECTION('',(0.866025403784439,0.,-0.5));
#13836=DIRECTION('center_axis',(0.,-1.,0.));
#13837=DIRECTION('ref_axis',(-8.88178419700125E-16,0.,1.));
#13838=DIRECTION('',(-1.1556266144132E-16,0.,-1.));
#13839=DIRECTION('center_axis',(0.,-1.,0.));
#13840=DIRECTION('ref_axis',(-8.88178419700125E-16,0.,1.));
#13841=DIRECTION('',(-0.866025403784438,0.,-0.5));
#13842=DIRECTION('center_axis',(0.,-1.,0.));
#13843=DIRECTION('ref_axis',(0.,0.,1.));
#13844=DIRECTION('',(-0.866025403784439,0.,0.5));
#13845=DIRECTION('center_axis',(0.,-1.,0.));
#13846=DIRECTION('ref_axis',(0.,0.,1.));
#13847=DIRECTION('',(1.1556266144132E-16,0.,1.));
#13848=DIRECTION('center_axis',(0.,1.,0.));
#13849=DIRECTION('ref_axis',(0.,0.,1.));
#13850=DIRECTION('center_axis',(-1.,0.,1.1556266144132E-16));
#13851=DIRECTION('ref_axis',(1.1556266144132E-16,0.,1.));
#13852=DIRECTION('',(0.,-1.,0.));
#13853=DIRECTION('',(0.,-1.,0.));
#13854=DIRECTION('center_axis',(-0.5,0.,0.866025403784439));
#13855=DIRECTION('ref_axis',(0.866025403784439,0.,0.5));
#13856=DIRECTION('',(0.,-1.,0.));
#13857=DIRECTION('center_axis',(0.5,0.,0.866025403784439));
#13858=DIRECTION('ref_axis',(0.866025403784439,0.,-0.5));
#13859=DIRECTION('',(0.,-1.,0.));
#13860=DIRECTION('center_axis',(1.,0.,-1.1556266144132E-16));
#13861=DIRECTION('ref_axis',(-1.1556266144132E-16,0.,-1.));
#13862=DIRECTION('',(0.,-1.,0.));
#13863=DIRECTION('center_axis',(0.5,0.,-0.866025403784439));
#13864=DIRECTION('ref_axis',(-0.866025403784439,0.,-0.5));
#13865=DIRECTION('',(0.,-1.,0.));
#13866=DIRECTION('center_axis',(-0.5,0.,-0.866025403784439));
#13867=DIRECTION('ref_axis',(-0.866025403784439,0.,0.5));
#13868=DIRECTION('center_axis',(0.,-1.,0.));
#13869=DIRECTION('ref_axis',(1.89882151931499E-15,0.,1.));
#13870=DIRECTION('center_axis',(0.,-1.,0.));
#13871=DIRECTION('ref_axis',(0.,0.,-1.));
#13872=DIRECTION('center_axis',(0.,-1.,0.));
#13873=DIRECTION('ref_axis',(0.,0.,-1.));
#13874=DIRECTION('center_axis',(0.,-1.,0.));
#13875=DIRECTION('ref_axis',(0.,0.,-1.));
#13876=DIRECTION('center_axis',(0.,-1.,0.));
#13877=DIRECTION('ref_axis',(0.,0.,-1.));
#13878=DIRECTION('center_axis',(0.,-1.,0.));
#13879=DIRECTION('ref_axis',(0.,0.,-1.));
#13880=DIRECTION('center_axis',(0.,1.,0.));
#13881=DIRECTION('ref_axis',(2.9861597890357E-15,0.,1.));
#13882=DIRECTION('center_axis',(0.,1.,0.));
#13883=DIRECTION('ref_axis',(0.,0.,-1.));
#13884=DIRECTION('center_axis',(0.,1.,0.));
#13885=DIRECTION('ref_axis',(0.,0.,-1.));
#13886=DIRECTION('center_axis',(0.,1.,0.));
#13887=DIRECTION('ref_axis',(0.,0.,-1.));
#13888=DIRECTION('center_axis',(0.,1.,0.));
#13889=DIRECTION('ref_axis',(0.,0.,-1.));
#13890=DIRECTION('center_axis',(0.,1.,0.));
#13891=DIRECTION('ref_axis',(0.,0.,-1.));
#13892=DIRECTION('center_axis',(0.,-1.,0.));
#13893=DIRECTION('ref_axis',(0.,0.,-1.));
#13894=DIRECTION('',(0.,-1.,0.));
#32778=CARTESIAN_POINT('',(0.,0.,0.));
#32779=CARTESIAN_POINT('Origin',(0.,-3.25,0.));
#32780=CARTESIAN_POINT('',(-3.48274395975477,-3.25,5.49479033678217));
#32781=CARTESIAN_POINT('',(-3.01725604024523,-3.25,5.76353991241553));
#32782=CARTESIAN_POINT('',(-6.5,-3.25,3.75277674973257));
#32783=CARTESIAN_POINT('',(-6.5,-3.25,0.268749575633325));
#32784=CARTESIAN_POINT('Origin',(0.,-3.25,0.));
#32785=CARTESIAN_POINT('',(-6.5,-3.25,-0.268749575633324));
#32786=CARTESIAN_POINT('',(-6.5,-3.25,-3.75277674973257));
#32787=CARTESIAN_POINT('',(-3.48274395975469,-3.25,-5.49479033678222));
#32788=CARTESIAN_POINT('Origin',(0.,-3.25,0.));
#32789=CARTESIAN_POINT('',(-3.01725604024531,-3.25,-5.76353991241548));
#32790=CARTESIAN_POINT('',(-2.05562859610134E-16,-3.25,-7.50555349946514));
#32791=CARTESIAN_POINT('',(3.01725604024528,-3.25,-5.7635399124155));
#32792=CARTESIAN_POINT('Origin',(0.,-3.25,0.));
#32793=CARTESIAN_POINT('',(3.48274395975473,-3.25,-5.4947903367822));
#32794=CARTESIAN_POINT('',(6.5,-3.25,-3.75277674973257));
#32795=CARTESIAN_POINT('',(6.5,-3.25,-0.26874957563335));
#32796=CARTESIAN_POINT('Origin',(0.,-3.25,0.));
#32797=CARTESIAN_POINT('',(6.5,-3.25,0.268749575633349));
#32798=CARTESIAN_POINT('',(6.5,-3.25,3.75277674973257));
#32799=CARTESIAN_POINT('',(3.48274395975475,-3.25,5.49479033678219));
#32800=CARTESIAN_POINT('Origin',(0.,-3.25,0.));
#32801=CARTESIAN_POINT('',(3.01725604024525,-3.25,5.76353991241551));
#32802=CARTESIAN_POINT('',(-5.5631874730702E-16,-3.25,7.50555349946513));
#32803=CARTESIAN_POINT('Origin',(0.,-3.25,0.));
#32804=CARTESIAN_POINT('',(0.0048323552597593,-3.25,3.49158803373809));
#32805=CARTESIAN_POINT('Origin',(0.00483235525975973,-3.25,-0.00841196626190816));
#32806=CARTESIAN_POINT('Origin',(0.,3.25,0.));
#32807=CARTESIAN_POINT('',(-3.48274395975477,3.25,5.49479033678217));
#32808=CARTESIAN_POINT('',(-6.5,3.25,0.268749575633325));
#32809=CARTESIAN_POINT('Origin',(0.,3.25,0.));
#32810=CARTESIAN_POINT('',(-3.01725604024523,3.25,5.76353991241552));
#32811=CARTESIAN_POINT('',(-6.5,3.25,3.75277674973257));
#32812=CARTESIAN_POINT('',(3.01725604024525,3.25,5.76353991241551));
#32813=CARTESIAN_POINT('Origin',(0.,3.25,0.));
#32814=CARTESIAN_POINT('',(3.48274395975475,3.25,5.49479033678219));
#32815=CARTESIAN_POINT('',(-5.5631874730702E-16,3.25,7.50555349946513));
#32816=CARTESIAN_POINT('',(6.5,3.25,0.268749575633349));
#32817=CARTESIAN_POINT('Origin',(0.,3.25,0.));
#32818=CARTESIAN_POINT('',(6.5,3.25,-0.26874957563335));
#32819=CARTESIAN_POINT('',(6.5,3.25,3.75277674973257));
#32820=CARTESIAN_POINT('',(3.48274395975473,3.25,-5.4947903367822));
#32821=CARTESIAN_POINT('Origin',(0.,3.25,0.));
#32822=CARTESIAN_POINT('',(3.01725604024528,3.25,-5.7635399124155));
#32823=CARTESIAN_POINT('',(6.5,3.25,-3.75277674973257));
#32824=CARTESIAN_POINT('',(-3.01725604024531,3.25,-5.76353991241549));
#32825=CARTESIAN_POINT('Origin',(0.,3.25,0.));
#32826=CARTESIAN_POINT('',(-3.48274395975469,3.25,-5.49479033678222));
#32827=CARTESIAN_POINT('',(-2.05562859610134E-16,3.25,-7.50555349946514));
#32828=CARTESIAN_POINT('',(-6.5,3.25,-0.268749575633324));
#32829=CARTESIAN_POINT('Origin',(0.,3.25,0.));
#32830=CARTESIAN_POINT('',(-6.5,3.25,-3.75277674973257));
#32831=CARTESIAN_POINT('',(0.00483235525975973,3.25,3.49158803373809));
#32832=CARTESIAN_POINT('Origin',(0.00483235525975973,3.25,-0.00841196626190816));
#32833=CARTESIAN_POINT('Origin',(6.5,3.25,3.75277674973257));
#32834=CARTESIAN_POINT('',(6.5,2.25,3.75277674973257));
#32835=CARTESIAN_POINT('',(6.5,-2.25,3.75277674973257));
#32836=CARTESIAN_POINT('',(6.5,3.25,3.75277674973257));
#32837=CARTESIAN_POINT('Ctrl Pts',(6.5,-2.25000000000019,3.75277674973218));
#32838=CARTESIAN_POINT('Ctrl Pts',(6.5,-3.18317224509129,1.88643225954984));
#32839=CARTESIAN_POINT('Ctrl Pts',(6.5,-3.25000000000011,0.268749575630723));
#32840=CARTESIAN_POINT('',(6.5,-2.25,-3.75277674973257));
#32841=CARTESIAN_POINT('Ctrl Pts',(6.5,-3.25000000000011,-0.268749575630739));
#32842=CARTESIAN_POINT('Ctrl Pts',(6.5,-3.18317224509129,-1.88643225954986));
#32843=CARTESIAN_POINT('Ctrl Pts',(6.5,-2.25000000000019,-3.7527767497322));
#32844=CARTESIAN_POINT('',(6.5,2.25,-3.75277674973257));
#32845=CARTESIAN_POINT('',(6.5,3.25,-3.75277674973257));
#32846=CARTESIAN_POINT('Ctrl Pts',(6.5,2.25000000000018,-3.75277674973221));
#32847=CARTESIAN_POINT('Ctrl Pts',(6.5,3.18317224509129,-1.88643225954986));
#32848=CARTESIAN_POINT('Ctrl Pts',(6.5,3.25000000000011,-0.268749575630731));
#32849=CARTESIAN_POINT('Ctrl Pts',(6.5,3.25000000000011,0.268749575630733));
#32850=CARTESIAN_POINT('Ctrl Pts',(6.5,3.18317224509129,1.88643225954985));
#32851=CARTESIAN_POINT('Ctrl Pts',(6.5,2.25000000000019,3.75277674973219));
#32852=CARTESIAN_POINT('Origin',(6.5,3.25,-3.75277674973257));
#32853=CARTESIAN_POINT('Ctrl Pts',(6.49999999999967,-2.25000000000019,-3.75277674973276));
#32854=CARTESIAN_POINT('Ctrl Pts',(4.88369825928862,-3.18317224509131,-4.68594899482394));
#32855=CARTESIAN_POINT('Ctrl Pts',(3.48274395975245,-3.25000000000011,-5.49479033678352));
#32856=CARTESIAN_POINT('',(-1.73472347597681E-15,-2.25,-7.50555349946514));
#32857=CARTESIAN_POINT('Ctrl Pts',(3.01725604024755,-3.25000000000011,-5.76353991241419));
#32858=CARTESIAN_POINT('Ctrl Pts',(1.61630174071138,-3.1831722450913,-6.57238125437376));
#32859=CARTESIAN_POINT('Ctrl Pts',(3.27578534860098E-13,-2.25000000000019,
-7.50555349946495));
#32860=CARTESIAN_POINT('',(-1.73472347597681E-15,2.25,-7.50555349946514));
#32861=CARTESIAN_POINT('',(-2.05562859610134E-16,3.25,-7.50555349946514));
#32862=CARTESIAN_POINT('Ctrl Pts',(3.28190693931138E-13,2.25000000000019,
-7.50555349946495));
#32863=CARTESIAN_POINT('Ctrl Pts',(1.61630174071138,3.1831722450913,-6.57238125437376));
#32864=CARTESIAN_POINT('Ctrl Pts',(3.01725604024755,3.25000000000011,-5.76353991241419));
#32865=CARTESIAN_POINT('Ctrl Pts',(3.48274395975246,3.25000000000011,-5.49479033678351));
#32866=CARTESIAN_POINT('Ctrl Pts',(4.88369825928863,3.1831722450913,-4.68594899482394));
#32867=CARTESIAN_POINT('Ctrl Pts',(6.49999999999968,2.25000000000019,-3.75277674973275));
#32868=CARTESIAN_POINT('Origin',(-2.05562859610134E-16,3.25,-7.50555349946514));
#32869=CARTESIAN_POINT('Ctrl Pts',(-3.25455340652671E-13,-2.25000000000019,
-7.50555349946495));
#32870=CARTESIAN_POINT('Ctrl Pts',(-1.61630174071139,-3.18317224509132,
-6.57238125437375));
#32871=CARTESIAN_POINT('Ctrl Pts',(-3.01725604024758,-3.25000000000011,
-5.76353991241417));
#32872=CARTESIAN_POINT('',(-6.5,-2.25,-3.75277674973257));
#32873=CARTESIAN_POINT('Ctrl Pts',(-3.48274395975242,-3.25000000000011,
-5.49479033678353));
#32874=CARTESIAN_POINT('Ctrl Pts',(-4.88369825928861,-3.18317224509131,
-4.68594899482395));
#32875=CARTESIAN_POINT('Ctrl Pts',(-6.49999999999967,-2.25000000000019,
-3.75277674973276));
#32876=CARTESIAN_POINT('',(-6.5,2.25,-3.75277674973257));
#32877=CARTESIAN_POINT('',(-6.5,3.25,-3.75277674973257));
#32878=CARTESIAN_POINT('Ctrl Pts',(-6.49999999999968,2.25000000000018,-3.75277674973276));
#32879=CARTESIAN_POINT('Ctrl Pts',(-4.88369825928861,3.18317224509131,-4.68594899482395));
#32880=CARTESIAN_POINT('Ctrl Pts',(-3.48274395975242,3.25000000000011,-5.49479033678354));
#32881=CARTESIAN_POINT('Ctrl Pts',(-3.01725604024757,3.25000000000011,-5.76353991241418));
#32882=CARTESIAN_POINT('Ctrl Pts',(-1.61630174071139,3.18317224509131,-6.57238125437376));
#32883=CARTESIAN_POINT('Ctrl Pts',(-3.28190693931137E-13,2.25000000000019,
-7.50555349946495));
#32884=CARTESIAN_POINT('Origin',(-6.5,3.25,-3.75277674973257));
#32885=CARTESIAN_POINT('Ctrl Pts',(-6.5,-2.25000000000018,-3.7527767497322));
#32886=CARTESIAN_POINT('Ctrl Pts',(-6.5,-3.1831722450913,-1.88643225954984));
#32887=CARTESIAN_POINT('Ctrl Pts',(-6.5,-3.25000000000011,-0.268749575630697));
#32888=CARTESIAN_POINT('',(-6.5,-2.25,3.75277674973256));
#32889=CARTESIAN_POINT('Ctrl Pts',(-6.5,-3.25000000000011,0.268749575630706));
#32890=CARTESIAN_POINT('Ctrl Pts',(-6.5,-3.1831722450913,1.88643225954984));
#32891=CARTESIAN_POINT('Ctrl Pts',(-6.5,-2.25000000000019,3.75277674973219));
#32892=CARTESIAN_POINT('',(-6.5,2.25,3.75277674973256));
#32893=CARTESIAN_POINT('',(-6.5,3.25,3.75277674973257));
#32894=CARTESIAN_POINT('Ctrl Pts',(-6.5,2.25000000000019,3.75277674973219));
#32895=CARTESIAN_POINT('Ctrl Pts',(-6.5,3.1831722450913,1.88643225954984));
#32896=CARTESIAN_POINT('Ctrl Pts',(-6.5,3.25000000000011,0.268749575630717));
#32897=CARTESIAN_POINT('Ctrl Pts',(-6.5,3.25000000000011,-0.268749575630705));
#32898=CARTESIAN_POINT('Ctrl Pts',(-6.5,3.1831722450913,-1.88643225954984));
#32899=CARTESIAN_POINT('Ctrl Pts',(-6.5,2.25000000000019,-3.75277674973219));
#32900=CARTESIAN_POINT('Origin',(-6.5,3.25,3.75277674973257));
#32901=CARTESIAN_POINT('Ctrl Pts',(-6.49999999999968,-2.25000000000019,
3.75277674973275));
#32902=CARTESIAN_POINT('Ctrl Pts',(-4.88369825928865,-3.18317224509129,
4.68594899482393));
#32903=CARTESIAN_POINT('Ctrl Pts',(-3.4827439597525,-3.25000000000011,5.49479033678349));
#32904=CARTESIAN_POINT('',(-3.03576608295941E-15,-2.25,7.50555349946514));
#32905=CARTESIAN_POINT('Ctrl Pts',(-3.0172560402475,-3.25000000000011,5.76353991241422));
#32906=CARTESIAN_POINT('Ctrl Pts',(-1.61630174071135,-3.18317224509129,
6.57238125437378));
#32907=CARTESIAN_POINT('Ctrl Pts',(-3.26061967569079E-13,-2.25000000000019,
7.50555349946495));
#32908=CARTESIAN_POINT('',(-3.03576608295941E-15,2.25,7.50555349946514));
#32909=CARTESIAN_POINT('',(-5.5631874730702E-16,3.25,7.50555349946513));
#32910=CARTESIAN_POINT('Ctrl Pts',(-3.3274047249765E-13,2.25000000000019,
7.50555349946494));
#32911=CARTESIAN_POINT('Ctrl Pts',(-1.61630174071135,3.18317224509129,6.57238125437378));
#32912=CARTESIAN_POINT('Ctrl Pts',(-3.0172560402475,3.25000000000011,5.76353991241422));
#32913=CARTESIAN_POINT('Ctrl Pts',(-3.48274395975249,3.25000000000011,5.49479033678349));
#32914=CARTESIAN_POINT('Ctrl Pts',(-4.88369825928865,3.1831722450913,4.68594899482393));
#32915=CARTESIAN_POINT('Ctrl Pts',(-6.49999999999968,2.25000000000019,3.75277674973275));
#32916=CARTESIAN_POINT('Origin',(-5.5631874730702E-16,3.25,7.50555349946513));
#32917=CARTESIAN_POINT('Ctrl Pts',(3.2697190794369E-13,-2.25000000000019,
7.50555349946494));
#32918=CARTESIAN_POINT('Ctrl Pts',(1.61630174071137,-3.1831722450913,6.57238125437376));
#32919=CARTESIAN_POINT('Ctrl Pts',(3.01725604024753,-3.25000000000011,5.7635399124142));
#32920=CARTESIAN_POINT('Ctrl Pts',(3.48274395975248,-3.25000000000011,5.49479033678349));
#32921=CARTESIAN_POINT('Ctrl Pts',(4.88369825928864,-3.1831722450913,4.68594899482393));
#32922=CARTESIAN_POINT('Ctrl Pts',(6.49999999999968,-2.25000000000019,3.75277674973275));
#32923=CARTESIAN_POINT('Ctrl Pts',(6.49999999999967,2.25000000000019,3.75277674973275));
#32924=CARTESIAN_POINT('Ctrl Pts',(4.88369825928864,3.1831722450913,4.68594899482393));
#32925=CARTESIAN_POINT('Ctrl Pts',(3.48274395975247,3.25000000000011,5.4947903367835));
#32926=CARTESIAN_POINT('Ctrl Pts',(3.01725604024752,3.25000000000011,5.7635399124142));
#32927=CARTESIAN_POINT('Ctrl Pts',(1.61630174071136,3.1831722450913,6.57238125437377));
#32928=CARTESIAN_POINT('Ctrl Pts',(3.19394455369212E-13,2.25000000000019,
7.50555349946495));
#32929=CARTESIAN_POINT('Origin',(0.,3.25,0.));
#32930=CARTESIAN_POINT('Origin',(0.,3.25,0.));
#32931=CARTESIAN_POINT('Origin',(0.,3.25,0.));
#32932=CARTESIAN_POINT('Origin',(0.,3.25,0.));
#32933=CARTESIAN_POINT('Origin',(0.,3.25,0.));
#32934=CARTESIAN_POINT('Origin',(0.,3.25,0.));
#32935=CARTESIAN_POINT('Origin',(0.,-3.25,0.));
#32936=CARTESIAN_POINT('Origin',(0.,-3.25,0.));
#32937=CARTESIAN_POINT('Origin',(0.,-3.25,0.));
#32938=CARTESIAN_POINT('Origin',(0.,-3.25,0.));
#32939=CARTESIAN_POINT('Origin',(0.,-3.25,0.));
#32940=CARTESIAN_POINT('Origin',(0.,-3.25,0.));
#32941=CARTESIAN_POINT('Origin',(0.00483235525975973,-3.25,-0.00841196626190816));
#32942=CARTESIAN_POINT('',(0.0048323552597593,-3.25,3.49158803373809));
#32983=UNCERTAINTY_MEASURE_WITH_UNIT(LENGTH_MEASURE(0.01),#33017,
'DISTANCE_ACCURACY_VALUE',
'Maximum model space distance between geometric entities at asserted c
onnectivities');
#32984=UNCERTAINTY_MEASURE_WITH_UNIT(LENGTH_MEASURE(0.01),#33017,
'DISTANCE_ACCURACY_VALUE',
'Maximum model space distance between geometric entities at asserted c
onnectivities');
#33015=(
GEOMETRIC_REPRESENTATION_CONTEXT(3)
GLOBAL_UNCERTAINTY_ASSIGNED_CONTEXT((#32983))
GLOBAL_UNIT_ASSIGNED_CONTEXT((#33017,#33019,#33020))
REPRESENTATION_CONTEXT('','3D')
);
#33016=(
GEOMETRIC_REPRESENTATION_CONTEXT(3)
GLOBAL_UNCERTAINTY_ASSIGNED_CONTEXT((#32984))
GLOBAL_UNIT_ASSIGNED_CONTEXT((#33017,#33019,#33020))
REPRESENTATION_CONTEXT('','3D')
);
#33017=(
LENGTH_UNIT()
NAMED_UNIT(*)
SI_UNIT(.MILLI.,.METRE.)
);
#33019=(
NAMED_UNIT(*)
PLANE_ANGLE_UNIT()
SI_UNIT($,.RADIAN.)
);
#33020=(
NAMED_UNIT(*)
SI_UNIT($,.STERADIAN.)
SOLID_ANGLE_UNIT()
);
#33051=SHAPE_DEFINITION_REPRESENTATION(#33113,#33154);
#33113=PRODUCT_DEFINITION_SHAPE('',$,#33186);
#33154=SHAPE_REPRESENTATION('',(#11187),#33015);
#33155=PRODUCT_DEFINITION_CONTEXT('part definition',#33250,'design');
#33186=PRODUCT_DEFINITION('P_Torque Wrench_Handle Grip Drive Nut_1012',
'P_Torque Wrench_Handle Grip Drive Nut_1012',#33217,#33155);
#33217=PRODUCT_DEFINITION_FORMATION('',$,#33282);
#33250=APPLICATION_CONTEXT(
'Core Data for Automotive Mechanical Design Process');
#33251=PRODUCT_CONTEXT('part definition',#33250,'mechanical');
#33282=PRODUCT('P_Torque Wrench_Handle Grip Drive Nut_1012',
'P_Torque Wrench_Handle Grip Drive Nut_1012',$,(#33251));
#33289=PRESENTATION_STYLE_ASSIGNMENT((#33296));
#33296=SURFACE_STYLE_USAGE(.BOTH.,#33303);
#33303=SURFACE_SIDE_STYLE('',(#33310));
#33310=SURFACE_STYLE_FILL_AREA(#33317);
#33317=FILL_AREA_STYLE('Opaque(255,255,255)',(#33324));
#33324=FILL_AREA_STYLE_COLOUR('Opaque(255,255,255)',#33331);
#33331=COLOUR_RGB('Opaque(255,255,255)', 0.08235294, 0.09019608, 0.10196078);
ENDSEC;
END-ISO-10303-21;
